ISO-10303-21;
HEADER;
/* Generated by software containing ST-Developer
 * from STEP Tools, Inc. (www.steptools.com) 
 */

FILE_DESCRIPTION(
/* description */ ('Hand wheel with handle and shaft collar'),
/* implementation_level */ '2;1');

FILE_NAME(
/* name */ 'Inner ring (1).step',
/* time_stamp */ '2026-10-28T03:23:19-07:00',
/* author */ (''),
/* organization */ (''),
/* preprocessor_version */ 'ST-DEVELOPER v20.2',
/* originating_system */ 'Autodesk Translation Framework v15.17.0.0',
/* authorisation */ '');

FILE_SCHEMA (('AUTOMOTIVE_DESIGN { 1 0 10303 214 3 1 1 }'));
ENDSEC;

DATA;
#10=MECHANICAL_DESIGN_GEOMETRIC_PRESENTATION_REPRESENTATION('',(#426),#10510);
#299=TOROIDAL_SURFACE('',#6194,1.,0.247676);
#317=CONICAL_SURFACE('',#6205,0.53,0.785398163397448);
#318=CONICAL_SURFACE('',#6212,0.53,0.785398163397448);
#355=SHAPE_REPRESENTATION_RELATIONSHIP('SRR','None',#10674,#387);
#387=ADVANCED_BREP_SHAPE_REPRESENTATION('',(#471),#10501);
#426=STYLED_ITEM('',(#10908),#471);
#471=MANIFOLD_SOLID_BREP('Body1',#5327);
#583=FACE_BOUND('',#1425,.T.);
#584=FACE_BOUND('',#1428,.T.);
#730=PLANE('',#6207);
#731=PLANE('',#6210);
#1004=FACE_OUTER_BOUND('',#1420,.T.);
#1005=FACE_OUTER_BOUND('',#1421,.T.);
#1006=FACE_OUTER_BOUND('',#1422,.T.);
#1007=FACE_OUTER_BOUND('',#1423,.T.);
#1008=FACE_OUTER_BOUND('',#1424,.T.);
#1009=FACE_OUTER_BOUND('',#1426,.T.);
#1010=FACE_OUTER_BOUND('',#1427,.T.);
#1011=FACE_OUTER_BOUND('',#1429,.T.);
#1420=EDGE_LOOP('',(#4573,#4574,#4575,#4576,#4577,#4578));
#1421=EDGE_LOOP('',(#4579,#4580,#4581,#4582,#4583));
#1422=EDGE_LOOP('',(#4584,#4585,#4586,#4587));
#1423=EDGE_LOOP('',(#4588,#4589,#4590,#4591));
#1424=EDGE_LOOP('',(#4592));
#1425=EDGE_LOOP('',(#4593));
#1426=EDGE_LOOP('',(#4594,#4595,#4596,#4597,#4598));
#1427=EDGE_LOOP('',(#4599));
#1428=EDGE_LOOP('',(#4600));
#1429=EDGE_LOOP('',(#4601,#4602,#4603,#4604));
#1778=LINE('',#9709,#2088);
#1779=LINE('',#9715,#2089);
#1780=LINE('',#9719,#2090);
#1781=LINE('',#9725,#2091);
#1782=LINE('',#9730,#2092);
#2088=VECTOR('',#7692,0.976185);
#2089=VECTOR('',#7699,0.5);
#2090=VECTOR('',#7704,0.53);
#2091=VECTOR('',#7713,0.976185);
#2092=VECTOR('',#7720,0.53);
#2354=CIRCLE('',#6195,0.976185);
#2355=CIRCLE('',#6196,0.976185);
#2356=CIRCLE('',#6197,0.247676);
#2357=CIRCLE('',#6198,0.976185);
#2358=CIRCLE('',#6199,0.976185);
#2359=CIRCLE('',#6201,0.976185);
#2360=CIRCLE('',#6203,0.5);
#2361=CIRCLE('',#6204,0.5);
#2362=CIRCLE('',#6206,0.56);
#2363=CIRCLE('',#6209,0.976185);
#2364=CIRCLE('',#6211,0.56);
#2786=VERTEX_POINT('',#9698);
#2787=VERTEX_POINT('',#9699);
#2788=VERTEX_POINT('',#9702);
#2789=VERTEX_POINT('',#9704);
#2790=VERTEX_POINT('',#9708);
#2791=VERTEX_POINT('',#9712);
#2792=VERTEX_POINT('',#9714);
#2793=VERTEX_POINT('',#9718);
#2794=VERTEX_POINT('',#9723);
#2795=VERTEX_POINT('',#9727);
#3404=EDGE_CURVE('',#2786,#2787,#2354,.T.);
#3405=EDGE_CURVE('',#2787,#2786,#2355,.T.);
#3406=EDGE_CURVE('',#2787,#2788,#2356,.T.);
#3407=EDGE_CURVE('',#2789,#2788,#2357,.T.);
#3408=EDGE_CURVE('',#2788,#2789,#2358,.T.);
#3409=EDGE_CURVE('',#2789,#2790,#1778,.T.);
#3410=EDGE_CURVE('',#2790,#2790,#2359,.T.);
#3411=EDGE_CURVE('',#2791,#2791,#2360,.T.);
#3412=EDGE_CURVE('',#2791,#2792,#1779,.T.);
#3413=EDGE_CURVE('',#2792,#2792,#2361,.T.);
#3414=EDGE_CURVE('',#2792,#2793,#1780,.T.);
#3415=EDGE_CURVE('',#2793,#2793,#2362,.T.);
#3416=EDGE_CURVE('',#2794,#2794,#2363,.T.);
#3417=EDGE_CURVE('',#2794,#2786,#1781,.T.);
#3418=EDGE_CURVE('',#2795,#2795,#2364,.T.);
#3419=EDGE_CURVE('',#2795,#2791,#1782,.T.);
#4573=ORIENTED_EDGE('',*,*,#3404,.F.);
#4574=ORIENTED_EDGE('',*,*,#3405,.F.);
#4575=ORIENTED_EDGE('',*,*,#3406,.T.);
#4576=ORIENTED_EDGE('',*,*,#3407,.F.);
#4577=ORIENTED_EDGE('',*,*,#3408,.F.);
#4578=ORIENTED_EDGE('',*,*,#3406,.F.);
#4579=ORIENTED_EDGE('',*,*,#3407,.T.);
#4580=ORIENTED_EDGE('',*,*,#3408,.T.);
#4581=ORIENTED_EDGE('',*,*,#3409,.T.);
#4582=ORIENTED_EDGE('',*,*,#3410,.T.);
#4583=ORIENTED_EDGE('',*,*,#3409,.F.);
#4584=ORIENTED_EDGE('',*,*,#3411,.T.);
#4585=ORIENTED_EDGE('',*,*,#3412,.T.);
#4586=ORIENTED_EDGE('',*,*,#3413,.F.);
#4587=ORIENTED_EDGE('',*,*,#3412,.F.);
#4588=ORIENTED_EDGE('',*,*,#3413,.T.);
#4589=ORIENTED_EDGE('',*,*,#3414,.T.);
#4590=ORIENTED_EDGE('',*,*,#3415,.F.);
#4591=ORIENTED_EDGE('',*,*,#3414,.F.);
#4592=ORIENTED_EDGE('',*,*,#3410,.F.);
#4593=ORIENTED_EDGE('',*,*,#3415,.T.);
#4594=ORIENTED_EDGE('',*,*,#3416,.F.);
#4595=ORIENTED_EDGE('',*,*,#3417,.T.);
#4596=ORIENTED_EDGE('',*,*,#3404,.T.);
#4597=ORIENTED_EDGE('',*,*,#3405,.T.);
#4598=ORIENTED_EDGE('',*,*,#3417,.F.);
#4599=ORIENTED_EDGE('',*,*,#3416,.T.);
#4600=ORIENTED_EDGE('',*,*,#3418,.F.);
#4601=ORIENTED_EDGE('',*,*,#3418,.T.);
#4602=ORIENTED_EDGE('',*,*,#3419,.T.);
#4603=ORIENTED_EDGE('',*,*,#3411,.F.);
#4604=ORIENTED_EDGE('',*,*,#3419,.F.);
#4956=CYLINDRICAL_SURFACE('',#6200,0.976185);
#4957=CYLINDRICAL_SURFACE('',#6202,0.5);
#4958=CYLINDRICAL_SURFACE('',#6208,0.976185);
#5216=ADVANCED_FACE('',(#1004),#299,.F.);
#5217=ADVANCED_FACE('',(#1005),#4956,.T.);
#5218=ADVANCED_FACE('',(#1006),#4957,.F.);
#5219=ADVANCED_FACE('',(#1007),#317,.F.);
#5220=ADVANCED_FACE('',(#1008,#583),#730,.T.);
#5221=ADVANCED_FACE('',(#1009),#4958,.T.);
#5222=ADVANCED_FACE('',(#1010,#584),#731,.T.);
#5223=ADVANCED_FACE('',(#1011),#318,.F.);
#5327=CLOSED_SHELL('',(#5216,#5217,#5218,#5219,#5220,#5221,#5222,#5223));
#6193=AXIS2_PLACEMENT_3D('',#9696,#7676,#7677);
#6194=AXIS2_PLACEMENT_3D('',#9697,#7678,#7679);
#6195=AXIS2_PLACEMENT_3D('',#9700,#7680,#7681);
#6196=AXIS2_PLACEMENT_3D('',#9701,#7682,#7683);
#6197=AXIS2_PLACEMENT_3D('',#9703,#7684,#7685);
#6198=AXIS2_PLACEMENT_3D('',#9705,#7686,#7687);
#6199=AXIS2_PLACEMENT_3D('',#9706,#7688,#7689);
#6200=AXIS2_PLACEMENT_3D('',#9707,#7690,#7691);
#6201=AXIS2_PLACEMENT_3D('',#9710,#7693,#7694);
#6202=AXIS2_PLACEMENT_3D('',#9711,#7695,#7696);
#6203=AXIS2_PLACEMENT_3D('',#9713,#7697,#7698);
#6204=AXIS2_PLACEMENT_3D('',#9716,#7700,#7701);
#6205=AXIS2_PLACEMENT_3D('',#9717,#7702,#7703);
#6206=AXIS2_PLACEMENT_3D('',#9720,#7705,#7706);
#6207=AXIS2_PLACEMENT_3D('',#9721,#7707,#7708);
#6208=AXIS2_PLACEMENT_3D('',#9722,#7709,#7710);
#6209=AXIS2_PLACEMENT_3D('',#9724,#7711,#7712);
#6210=AXIS2_PLACEMENT_3D('',#9726,#7714,#7715);
#6211=AXIS2_PLACEMENT_3D('',#9728,#7716,#7717);
#6212=AXIS2_PLACEMENT_3D('',#9729,#7718,#7719);
#7676=DIRECTION('axis',(0.,0.,1.));
#7677=DIRECTION('refdir',(1.,0.,0.));
#7678=DIRECTION('center_axis',(0.,-1.,0.));
#7679=DIRECTION('ref_axis',(0.,0.,-1.));
#7680=DIRECTION('center_axis',(0.,-1.,0.));
#7681=DIRECTION('ref_axis',(1.,0.,0.));
#7682=DIRECTION('center_axis',(0.,-1.,0.));
#7683=DIRECTION('ref_axis',(1.,0.,0.));
#7684=DIRECTION('center_axis',(1.,0.,1.22464679914735E-16));
#7685=DIRECTION('ref_axis',(-1.22464679914735E-16,0.,1.));
#7686=DIRECTION('center_axis',(0.,1.,0.));
#7687=DIRECTION('ref_axis',(1.,0.,0.));
#7688=DIRECTION('center_axis',(0.,1.,0.));
#7689=DIRECTION('ref_axis',(1.,0.,0.));
#7690=DIRECTION('center_axis',(0.,-1.,0.));
#7691=DIRECTION('ref_axis',(1.,0.,0.));
#7692=DIRECTION('',(0.,1.,0.));
#7693=DIRECTION('center_axis',(0.,-1.,0.));
#7694=DIRECTION('ref_axis',(1.,0.,0.));
#7695=DIRECTION('center_axis',(0.,-1.,0.));
#7696=DIRECTION('ref_axis',(1.,0.,0.));
#7697=DIRECTION('center_axis',(0.,-1.,0.));
#7698=DIRECTION('ref_axis',(1.,0.,0.));
#7699=DIRECTION('',(0.,1.,0.));
#7700=DIRECTION('center_axis',(0.,-1.,0.));
#7701=DIRECTION('ref_axis',(1.,0.,0.));
#7702=DIRECTION('center_axis',(0.,1.,0.));
#7703=DIRECTION('ref_axis',(1.,0.,0.));
#7704=DIRECTION('',(-0.707106781186547,0.707106781186548,-8.65956056235493E-17));
#7705=DIRECTION('center_axis',(0.,-1.,0.));
#7706=DIRECTION('ref_axis',(1.,0.,0.));
#7707=DIRECTION('center_axis',(0.,1.,0.));
#7708=DIRECTION('ref_axis',(0.,0.,1.));
#7709=DIRECTION('center_axis',(0.,-1.,0.));
#7710=DIRECTION('ref_axis',(1.,0.,0.));
#7711=DIRECTION('center_axis',(0.,-1.,0.));
#7712=DIRECTION('ref_axis',(1.,0.,0.));
#7713=DIRECTION('',(0.,1.,0.));
#7714=DIRECTION('center_axis',(0.,-1.,0.));
#7715=DIRECTION('ref_axis',(0.,0.,-1.));
#7716=DIRECTION('center_axis',(0.,-1.,0.));
#7717=DIRECTION('ref_axis',(1.,0.,0.));
#7718=DIRECTION('center_axis',(0.,-1.,0.));
#7719=DIRECTION('ref_axis',(1.,0.,0.));
#7720=DIRECTION('',(0.707106781186547,0.707106781186548,8.65956056235493E-17));
#9696=CARTESIAN_POINT('',(0.,0.,0.));
#9697=CARTESIAN_POINT('Origin',(0.,0.,0.));
#9698=CARTESIAN_POINT('',(-0.976185,-0.246528389340863,-1.19548183562566E-16));
#9699=CARTESIAN_POINT('',(-1.19548183562566E-16,-0.246528389340863,0.976185));
#9700=CARTESIAN_POINT('Origin',(0.,-0.246528389340863,0.));
#9701=CARTESIAN_POINT('Origin',(0.,-0.246528389340863,0.));
#9702=CARTESIAN_POINT('',(-1.19548183562566E-16,0.246528389340863,0.976185));
#9703=CARTESIAN_POINT('Origin',(-1.22464679914735E-16,0.,1.));
#9704=CARTESIAN_POINT('',(-0.976185,0.246528389340863,1.19548183562566E-16));
#9705=CARTESIAN_POINT('Origin',(0.,0.246528389340863,0.));
#9706=CARTESIAN_POINT('Origin',(0.,0.246528389340863,0.));
#9707=CARTESIAN_POINT('Origin',(0.,0.,0.));
#9708=CARTESIAN_POINT('',(-0.976185,0.45,-1.19548183562566E-16));
#9709=CARTESIAN_POINT('',(-0.976185,0.,-1.19548183562566E-16));
#9710=CARTESIAN_POINT('Origin',(0.,0.45,0.));
#9711=CARTESIAN_POINT('Origin',(0.,0.,0.));
#9712=CARTESIAN_POINT('',(-0.5,-0.39,-6.12323399573677E-17));
#9713=CARTESIAN_POINT('Origin',(0.,-0.39,0.));
#9714=CARTESIAN_POINT('',(-0.5,0.39,-6.12323399573677E-17));
#9715=CARTESIAN_POINT('',(-0.5,0.,-6.12323399573677E-17));
#9716=CARTESIAN_POINT('Origin',(0.,0.39,0.));
#9717=CARTESIAN_POINT('Origin',(0.,0.42,0.));
#9718=CARTESIAN_POINT('',(-0.56,0.45,-6.85802207522518E-17));
#9719=CARTESIAN_POINT('',(-0.53,0.42,-6.49062803548097E-17));
#9720=CARTESIAN_POINT('Origin',(0.,0.45,0.));
#9721=CARTESIAN_POINT('Origin',(0.976185,0.45,0.));
#9722=CARTESIAN_POINT('Origin',(0.,0.,0.));
#9723=CARTESIAN_POINT('',(-0.976185,-0.45,-1.19548183562566E-16));
#9724=CARTESIAN_POINT('Origin',(0.,-0.45,0.));
#9725=CARTESIAN_POINT('',(-0.976185,0.,-1.19548183562566E-16));
#9726=CARTESIAN_POINT('Origin',(0.56,-0.45,0.));
#9727=CARTESIAN_POINT('',(-0.56,-0.45,-6.85802207522518E-17));
#9728=CARTESIAN_POINT('Origin',(0.,-0.45,0.));
#9729=CARTESIAN_POINT('Origin',(0.,-0.42,0.));
#9730=CARTESIAN_POINT('',(-0.53,-0.42,-6.49062803548097E-17));
#10462=UNCERTAINTY_MEASURE_WITH_UNIT(LENGTH_MEASURE(0.001),#10511,
'DISTANCE_ACCURACY_VALUE',
'Maximum model space distance between geometric entities at asserted c
onnectivities');
#10471=UNCERTAINTY_MEASURE_WITH_UNIT(LENGTH_MEASURE(0.001),#10511,
'DISTANCE_ACCURACY_VALUE',
'Maximum model space distance between geometric entities at asserted c
onnectivities');
#10501=(
GEOMETRIC_REPRESENTATION_CONTEXT(3)
GLOBAL_UNCERTAINTY_ASSIGNED_CONTEXT((#10462))
GLOBAL_UNIT_ASSIGNED_CONTEXT((#10511,#10513,#10514))
REPRESENTATION_CONTEXT('','3D')
);
#10510=(
GEOMETRIC_REPRESENTATION_CONTEXT(3)
GLOBAL_UNCERTAINTY_ASSIGNED_CONTEXT((#10471))
GLOBAL_UNIT_ASSIGNED_CONTEXT((#10511,#10513,#10514))
REPRESENTATION_CONTEXT('','3D')
);
#10511=(
LENGTH_UNIT()
NAMED_UNIT(*)
SI_UNIT(.CENTI.,.METRE.)
);
#10513=(
NAMED_UNIT(*)
PLANE_ANGLE_UNIT()
SI_UNIT($,.RADIAN.)
);
#10514=(
NAMED_UNIT(*)
SI_UNIT($,.STERADIAN.)
SOLID_ANGLE_UNIT()
);
#10544=SHAPE_DEFINITION_REPRESENTATION(#10587,#10674);
#10587=PRODUCT_DEFINITION_SHAPE('',$,#10713);
#10674=SHAPE_REPRESENTATION('',(#6193),#10501);
#10683=PRODUCT_DEFINITION_CONTEXT('part definition',#10799,'design');
#10713=PRODUCT_DEFINITION('Inner ring (1)','Inner ring (1)',#10751,#10683);
#10751=PRODUCT_DEFINITION_FORMATION('',$,#10830);
#10799=APPLICATION_CONTEXT(
'Core Data for Automotive Mechanical Design Process');
#10800=PRODUCT_CONTEXT('part definition',#10799,'mechanical');
#10830=PRODUCT('Inner ring (1)','Inner ring (1)','Inner ring (1)',(#10800));
#10902=COLOUR_RGB('Grey',0.48,0.52,0.57);
#10903=FILL_AREA_STYLE_COLOUR('',#10902);
#10904=FILL_AREA_STYLE('',(#10903));
#10905=SURFACE_STYLE_FILL_AREA(#10904);
#10906=SURFACE_SIDE_STYLE('',(#10905));
#10907=SURFACE_STYLE_USAGE(.BOTH.,#10906);
#10908=PRESENTATION_STYLE_ASSIGNMENT((#10907));
ENDSEC;
END-ISO-10303-21;
